ISO-10303-21;
HEADER;
/* Generated by software containing ST-Developer
 * from STEP Tools, Inc. (www.steptools.com) 
 */

FILE_DESCRIPTION(
/* description */ ('Four-bar parallelogram arm'),
/* implementation_level */ '2;1');

FILE_NAME(
/* name */ 'Outer race spacer (1).step',
/* time_stamp */ '2026-10-28T03:24:55-07:00',
/* author */ (''),
/* organization */ (''),
/* preprocessor_version */ 'ST-DEVELOPER v20.2',
/* originating_system */ 'Autodesk Translation Framework v15.17.0.0',
/* authorisation */ '');

FILE_SCHEMA (('AUTOMOTIVE_DESIGN { 1 0 10303 214 3 1 1 }'));
ENDSEC;

DATA;
#10=MECHANICAL_DESIGN_GEOMETRIC_PRESENTATION_REPRESENTATION('',(#643),#14512);
#543=SHAPE_REPRESENTATION_RELATIONSHIP('SRR','None',#14765,#593);
#593=ADVANCED_BREP_SHAPE_REPRESENTATION('',(#700),#14480);
#643=STYLED_ITEM('',(#15087),#700);
#700=MANIFOLD_SOLID_BREP('Body1',#7348);
#849=FACE_BOUND('',#1914,.T.);
#850=FACE_BOUND('',#1916,.T.);
#1099=PLANE('',#8308);
#1100=PLANE('',#8309);
#1377=FACE_OUTER_BOUND('',#1911,.T.);
#1378=FACE_OUTER_BOUND('',#1912,.T.);
#1379=FACE_OUTER_BOUND('',#1913,.T.);
#1380=FACE_OUTER_BOUND('',#1915,.T.);
#1911=EDGE_LOOP('',(#5718,#5719,#5720,#5721));
#1912=EDGE_LOOP('',(#5722,#5723,#5724,#5725));
#1913=EDGE_LOOP('',(#5726));
#1914=EDGE_LOOP('',(#5727));
#1915=EDGE_LOOP('',(#5728));
#1916=EDGE_LOOP('',(#5729));
#2507=LINE('',#12841,#2901);
#2508=LINE('',#12847,#2902);
#2901=VECTOR('',#9897,1.02);
#2902=VECTOR('',#9904,1.49);
#3264=CIRCLE('',#8303,1.02);
#3265=CIRCLE('',#8304,1.02);
#3266=CIRCLE('',#8306,1.49);
#3267=CIRCLE('',#8307,1.49);
#3786=VERTEX_POINT('',#12838);
#3787=VERTEX_POINT('',#12840);
#3788=VERTEX_POINT('',#12844);
#3789=VERTEX_POINT('',#12846);
#4490=EDGE_CURVE('',#3786,#3786,#3264,.T.);
#4491=EDGE_CURVE('',#3786,#3787,#2507,.T.);
#4492=EDGE_CURVE('',#3787,#3787,#3265,.T.);
#4493=EDGE_CURVE('',#3788,#3788,#3266,.T.);
#4494=EDGE_CURVE('',#3788,#3789,#2508,.T.);
#4495=EDGE_CURVE('',#3789,#3789,#3267,.T.);
#5718=ORIENTED_EDGE('',*,*,#4490,.F.);
#5719=ORIENTED_EDGE('',*,*,#4491,.T.);
#5720=ORIENTED_EDGE('',*,*,#4492,.T.);
#5721=ORIENTED_EDGE('',*,*,#4491,.F.);
#5722=ORIENTED_EDGE('',*,*,#4493,.F.);
#5723=ORIENTED_EDGE('',*,*,#4494,.T.);
#5724=ORIENTED_EDGE('',*,*,#4495,.T.);
#5725=ORIENTED_EDGE('',*,*,#4494,.F.);
#5726=ORIENTED_EDGE('',*,*,#4493,.T.);
#5727=ORIENTED_EDGE('',*,*,#4490,.T.);
#5728=ORIENTED_EDGE('',*,*,#4495,.F.);
#5729=ORIENTED_EDGE('',*,*,#4492,.F.);
#6793=CYLINDRICAL_SURFACE('',#8302,1.02);
#6794=CYLINDRICAL_SURFACE('',#8305,1.49);
#7082=ADVANCED_FACE('',(#1377),#6793,.F.);
#7083=ADVANCED_FACE('',(#1378),#6794,.T.);
#7084=ADVANCED_FACE('',(#1379,#849),#1099,.T.);
#7085=ADVANCED_FACE('',(#1380,#850),#1100,.F.);
#7348=CLOSED_SHELL('',(#7082,#7083,#7084,#7085));
#8301=AXIS2_PLACEMENT_3D('',#12836,#9891,#9892);
#8302=AXIS2_PLACEMENT_3D('',#12837,#9893,#9894);
#8303=AXIS2_PLACEMENT_3D('',#12839,#9895,#9896);
#8304=AXIS2_PLACEMENT_3D('',#12842,#9898,#9899);
#8305=AXIS2_PLACEMENT_3D('',#12843,#9900,#9901);
#8306=AXIS2_PLACEMENT_3D('',#12845,#9902,#9903);
#8307=AXIS2_PLACEMENT_3D('',#12848,#9905,#9906);
#8308=AXIS2_PLACEMENT_3D('',#12849,#9907,#9908);
#8309=AXIS2_PLACEMENT_3D('',#12850,#9909,#9910);
#9891=DIRECTION('axis',(0.,0.,1.));
#9892=DIRECTION('refdir',(1.,0.,0.));
#9893=DIRECTION('center_axis',(0.,1.,0.));
#9894=DIRECTION('ref_axis',(1.,0.,0.));
#9895=DIRECTION('center_axis',(0.,-1.,0.));
#9896=DIRECTION('ref_axis',(1.,0.,0.));
#9897=DIRECTION('',(0.,-1.,0.));
#9898=DIRECTION('center_axis',(0.,-1.,0.));
#9899=DIRECTION('ref_axis',(1.,0.,0.));
#9900=DIRECTION('center_axis',(0.,1.,0.));
#9901=DIRECTION('ref_axis',(1.,0.,0.));
#9902=DIRECTION('center_axis',(0.,1.,0.));
#9903=DIRECTION('ref_axis',(1.,0.,0.));
#9904=DIRECTION('',(0.,-1.,0.));
#9905=DIRECTION('center_axis',(0.,1.,0.));
#9906=DIRECTION('ref_axis',(1.,0.,0.));
#9907=DIRECTION('center_axis',(0.,1.,0.));
#9908=DIRECTION('ref_axis',(1.,0.,0.));
#9909=DIRECTION('center_axis',(0.,1.,0.));
#9910=DIRECTION('ref_axis',(1.,0.,0.));
#12836=CARTESIAN_POINT('',(0.,0.,0.));
#12837=CARTESIAN_POINT('Origin',(20.,-0.15,8.));
#12838=CARTESIAN_POINT('',(18.98,0.15,8.));
#12839=CARTESIAN_POINT('Origin',(20.,0.15,8.));
#12840=CARTESIAN_POINT('',(18.98,-0.15,8.));
#12841=CARTESIAN_POINT('',(18.98,-0.15,8.));
#12842=CARTESIAN_POINT('Origin',(20.,-0.15,8.));
#12843=CARTESIAN_POINT('Origin',(20.,-0.15,8.));
#12844=CARTESIAN_POINT('',(18.51,0.15,8.));
#12845=CARTESIAN_POINT('Origin',(20.,0.15,8.));
#12846=CARTESIAN_POINT('',(18.51,-0.15,8.));
#12847=CARTESIAN_POINT('',(18.51,-0.15,8.));
#12848=CARTESIAN_POINT('Origin',(20.,-0.15,8.));
#12849=CARTESIAN_POINT('Origin',(20.,0.15,8.));
#12850=CARTESIAN_POINT('Origin',(20.,-0.15,8.));
#14423=UNCERTAINTY_MEASURE_WITH_UNIT(LENGTH_MEASURE(0.001),#14513,
'DISTANCE_ACCURACY_VALUE',
'Maximum model space distance between geometric entities at asserted c
onnectivities');
#14455=UNCERTAINTY_MEASURE_WITH_UNIT(LENGTH_MEASURE(0.001),#14513,
'DISTANCE_ACCURACY_VALUE',
'Maximum model space distance between geometric entities at asserted c
onnectivities');
#14480=(
GEOMETRIC_REPRESENTATION_CONTEXT(3)
GLOBAL_UNCERTAINTY_ASSIGNED_CONTEXT((#14423))
GLOBAL_UNIT_ASSIGNED_CONTEXT((#14513,#14515,#14516))
REPRESENTATION_CONTEXT('','3D')
);
#14512=(
GEOMETRIC_REPRESENTATION_CONTEXT(3)
GLOBAL_UNCERTAINTY_ASSIGNED_CONTEXT((#14455))
GLOBAL_UNIT_ASSIGNED_CONTEXT((#14513,#14515,#14516))
REPRESENTATION_CONTEXT('','3D')
);
#14513=(
LENGTH_UNIT()
NAMED_UNIT(*)
SI_UNIT(.CENTI.,.METRE.)
);
#14515=(
NAMED_UNIT(*)
PLANE_ANGLE_UNIT()
SI_UNIT($,.RADIAN.)
);
#14516=(
NAMED_UNIT(*)
SI_UNIT($,.STERADIAN.)
SOLID_ANGLE_UNIT()
);
#14541=SHAPE_DEFINITION_REPRESENTATION(#14597,#14765);
#14597=PRODUCT_DEFINITION_SHAPE('',$,#14822);
#14765=SHAPE_REPRESENTATION('',(#8301),#14480);
#14797=PRODUCT_DEFINITION_CONTEXT('part definition',#14967,'design');
#14822=PRODUCT_DEFINITION('Outer race spacer (1)','Outer race spacer (1)',
#14878,#14797);
#14878=PRODUCT_DEFINITION_FORMATION('',$,#14993);
#14967=APPLICATION_CONTEXT(
'Core Data for Automotive Mechanical Design Process');
#14968=PRODUCT_CONTEXT('part definition',#14967,'mechanical');
#14993=PRODUCT('Outer race spacer (1)','Outer race spacer (1)',
'Outer race spacer (1)',(#14968));
#15081=COLOUR_RGB('Grey',0.48,0.52,0.57);
#15082=FILL_AREA_STYLE_COLOUR('',#15081);
#15083=FILL_AREA_STYLE('',(#15082));
#15084=SURFACE_STYLE_FILL_AREA(#15083);
#15085=SURFACE_SIDE_STYLE('',(#15084));
#15086=SURFACE_STYLE_USAGE(.BOTH.,#15085);
#15087=PRESENTATION_STYLE_ASSIGNMENT((#15086));
ENDSEC;
END-ISO-10303-21;
